ISO-10303-21;
HEADER;
/* Generated by software containing ST-Developer
 * from STEP Tools, Inc. (www.steptools.com) 
 */

FILE_DESCRIPTION(
/* description */ ('Compact handwheel screw vise'),
/* implementation_level */ '2;1');

FILE_NAME(
/* name */ 'Cap Screw - M4x16.step',
/* time_stamp */ '2026-10-29T16:08:22-07:00',
/* author */ (''),
/* organization */ (''),
/* preprocessor_version */ 'ST-DEVELOPER v20.2',
/* originating_system */ 'Autodesk Translation Framework v15.17.0.0',
/* authorisation */ '');

FILE_SCHEMA (('AUTOMOTIVE_DESIGN { 1 0 10303 214 3 1 1 }'));
ENDSEC;

DATA;
#10=MECHANICAL_DESIGN_GEOMETRIC_PRESENTATION_REPRESENTATION('',(#669),#25074);
#570=CONICAL_SURFACE('',#8857,0.325,0.785398163397448);
#571=CONICAL_SURFACE('',#8861,0.335,0.785398163397448);
#572=CONICAL_SURFACE('',#8865,0.21,0.463647609000806);
#573=CONICAL_SURFACE('',#8869,0.18,0.785398163397448);
#582=ORIENTED_CLOSED_SHELL('',*,#8080,.F.);
#586=BREP_WITH_VOIDS('Body1',#8079,(#582));
#605=SHAPE_REPRESENTATION_RELATIONSHIP('SRR','None',#25215,#633);
#633=ADVANCED_BREP_SHAPE_REPRESENTATION('',(#586),#25062);
#669=STYLED_ITEM('',(#25446),#586);
#798=FACE_BOUND('',#1810,.T.);
#942=PLANE('',#8855);
#943=PLANE('',#8863);
#944=PLANE('',#8871);
#945=PLANE('',#8872);
#946=PLANE('',#8873);
#947=PLANE('',#8874);
#948=PLANE('',#8875);
#949=PLANE('',#8876);
#950=PLANE('',#8877);
#951=PLANE('',#8878);
#952=PLANE('',#8879);
#1249=FACE_OUTER_BOUND('',#1805,.T.);
#1250=FACE_OUTER_BOUND('',#1806,.T.);
#1251=FACE_OUTER_BOUND('',#1807,.T.);
#1252=FACE_OUTER_BOUND('',#1808,.T.);
#1253=FACE_OUTER_BOUND('',#1809,.T.);
#1254=FACE_OUTER_BOUND('',#1811,.T.);
#1255=FACE_OUTER_BOUND('',#1812,.T.);
#1256=FACE_OUTER_BOUND('',#1813,.T.);
#1257=FACE_OUTER_BOUND('',#1814,.T.);
#1258=FACE_OUTER_BOUND('',#1815,.T.);
#1259=FACE_OUTER_BOUND('',#1816,.T.);
#1260=FACE_OUTER_BOUND('',#1817,.T.);
#1261=FACE_OUTER_BOUND('',#1818,.T.);
#1262=FACE_OUTER_BOUND('',#1819,.T.);
#1263=FACE_OUTER_BOUND('',#1820,.T.);
#1264=FACE_OUTER_BOUND('',#1821,.T.);
#1265=FACE_OUTER_BOUND('',#1822,.T.);
#1805=EDGE_LOOP('',(#6155));
#1806=EDGE_LOOP('',(#6156,#6157,#6158,#6159));
#1807=EDGE_LOOP('',(#6160,#6161,#6162,#6163));
#1808=EDGE_LOOP('',(#6164,#6165,#6166,#6167));
#1809=EDGE_LOOP('',(#6168));
#1810=EDGE_LOOP('',(#6169));
#1811=EDGE_LOOP('',(#6170,#6171,#6172,#6173));
#1812=EDGE_LOOP('',(#6174,#6175,#6176,#6177));
#1813=EDGE_LOOP('',(#6178,#6179,#6180,#6181));
#1814=EDGE_LOOP('',(#6182));
#1815=EDGE_LOOP('',(#6183,#6184,#6185,#6186));
#1816=EDGE_LOOP('',(#6187,#6188,#6189,#6190));
#1817=EDGE_LOOP('',(#6191,#6192,#6193,#6194));
#1818=EDGE_LOOP('',(#6195,#6196,#6197,#6198));
#1819=EDGE_LOOP('',(#6199,#6200,#6201,#6202));
#1820=EDGE_LOOP('',(#6203,#6204,#6205,#6206));
#1821=EDGE_LOOP('',(#6207,#6208,#6209,#6210,#6211,#6212));
#1822=EDGE_LOOP('',(#6213,#6214,#6215,#6216,#6217,#6218));
#2307=LINE('',#14792,#2815);
#2308=LINE('',#14796,#2816);
#2309=LINE('',#14800,#2817);
#2310=LINE('',#14807,#2818);
#2311=LINE('',#14811,#2819);
#2312=LINE('',#14815,#2820);
#2313=LINE('',#14820,#2821);
#2314=LINE('',#14822,#2822);
#2315=LINE('',#14824,#2823);
#2316=LINE('',#14825,#2824);
#2317=LINE('',#14828,#2825);
#2318=LINE('',#14830,#2826);
#2319=LINE('',#14831,#2827);
#2320=LINE('',#14834,#2828);
#2321=LINE('',#14836,#2829);
#2322=LINE('',#14837,#2830);
#2323=LINE('',#14840,#2831);
#2324=LINE('',#14842,#2832);
#2325=LINE('',#14843,#2833);
#2326=LINE('',#14846,#2834);
#2327=LINE('',#14848,#2835);
#2328=LINE('',#14849,#2836);
#2329=LINE('',#14851,#2837);
#2330=LINE('',#14852,#2838);
#2815=VECTOR('',#10365,0.325);
#2816=VECTOR('',#10370,0.35);
#2817=VECTOR('',#10375,0.335);
#2818=VECTOR('',#10384,0.21);
#2819=VECTOR('',#10389,0.2);
#2820=VECTOR('',#10394,0.18);
#2821=VECTOR('',#10399,1.);
#2822=VECTOR('',#10400,1.);
#2823=VECTOR('',#10401,1.);
#2824=VECTOR('',#10402,1.);
#2825=VECTOR('',#10405,1.);
#2826=VECTOR('',#10406,1.);
#2827=VECTOR('',#10407,1.);
#2828=VECTOR('',#10410,1.);
#2829=VECTOR('',#10411,1.);
#2830=VECTOR('',#10412,1.);
#2831=VECTOR('',#10415,1.);
#2832=VECTOR('',#10416,1.);
#2833=VECTOR('',#10417,1.);
#2834=VECTOR('',#10420,1.);
#2835=VECTOR('',#10421,1.);
#2836=VECTOR('',#10422,1.);
#2837=VECTOR('',#10425,1.);
#2838=VECTOR('',#10426,1.);
#3270=CIRCLE('',#8856,0.3);
#3271=CIRCLE('',#8858,0.35);
#3272=CIRCLE('',#8860,0.35);
#3273=CIRCLE('',#8862,0.32);
#3274=CIRCLE('',#8864,0.22);
#3275=CIRCLE('',#8866,0.1954);
#3276=CIRCLE('',#8868,0.1954);
#3277=CIRCLE('',#8870,0.16);
#3672=VERTEX_POINT('',#14787);
#3673=VERTEX_POINT('',#14790);
#3674=VERTEX_POINT('',#14794);
#3675=VERTEX_POINT('',#14798);
#3676=VERTEX_POINT('',#14802);
#3677=VERTEX_POINT('',#14805);
#3678=VERTEX_POINT('',#14809);
#3679=VERTEX_POINT('',#14813);
#3680=VERTEX_POINT('',#14818);
#3681=VERTEX_POINT('',#14819);
#3682=VERTEX_POINT('',#14821);
#3683=VERTEX_POINT('',#14823);
#3684=VERTEX_POINT('',#14827);
#3685=VERTEX_POINT('',#14829);
#3686=VERTEX_POINT('',#14833);
#3687=VERTEX_POINT('',#14835);
#3688=VERTEX_POINT('',#14839);
#3689=VERTEX_POINT('',#14841);
#3690=VERTEX_POINT('',#14845);
#3691=VERTEX_POINT('',#14847);
#4564=EDGE_CURVE('',#3672,#3672,#3270,.T.);
#4565=EDGE_CURVE('',#3673,#3673,#3271,.T.);
#4566=EDGE_CURVE('',#3673,#3672,#2307,.T.);
#4567=EDGE_CURVE('',#3674,#3674,#3272,.T.);
#4568=EDGE_CURVE('',#3674,#3673,#2308,.T.);
#4569=EDGE_CURVE('',#3675,#3675,#3273,.T.);
#4570=EDGE_CURVE('',#3675,#3674,#2309,.T.);
#4571=EDGE_CURVE('',#3676,#3676,#3274,.T.);
#4572=EDGE_CURVE('',#3677,#3677,#3275,.F.);
#4573=EDGE_CURVE('',#3677,#3676,#2310,.T.);
#4574=EDGE_CURVE('',#3678,#3678,#3276,.F.);
#4575=EDGE_CURVE('',#3678,#3677,#2311,.T.);
#4576=EDGE_CURVE('',#3679,#3679,#3277,.T.);
#4577=EDGE_CURVE('',#3679,#3678,#2312,.T.);
#4578=EDGE_CURVE('',#3680,#3681,#2313,.T.);
#4579=EDGE_CURVE('',#3681,#3682,#2314,.T.);
#4580=EDGE_CURVE('',#3682,#3683,#2315,.T.);
#4581=EDGE_CURVE('',#3680,#3683,#2316,.T.);
#4582=EDGE_CURVE('',#3681,#3684,#2317,.T.);
#4583=EDGE_CURVE('',#3684,#3685,#2318,.T.);
#4584=EDGE_CURVE('',#3685,#3682,#2319,.T.);
#4585=EDGE_CURVE('',#3684,#3686,#2320,.T.);
#4586=EDGE_CURVE('',#3686,#3687,#2321,.T.);
#4587=EDGE_CURVE('',#3687,#3685,#2322,.T.);
#4588=EDGE_CURVE('',#3686,#3688,#2323,.T.);
#4589=EDGE_CURVE('',#3688,#3689,#2324,.T.);
#4590=EDGE_CURVE('',#3689,#3687,#2325,.T.);
#4591=EDGE_CURVE('',#3688,#3690,#2326,.T.);
#4592=EDGE_CURVE('',#3690,#3691,#2327,.T.);
#4593=EDGE_CURVE('',#3691,#3689,#2328,.T.);
#4594=EDGE_CURVE('',#3690,#3680,#2329,.T.);
#4595=EDGE_CURVE('',#3683,#3691,#2330,.T.);
#6155=ORIENTED_EDGE('',*,*,#4564,.F.);
#6156=ORIENTED_EDGE('',*,*,#4565,.F.);
#6157=ORIENTED_EDGE('',*,*,#4566,.T.);
#6158=ORIENTED_EDGE('',*,*,#4564,.T.);
#6159=ORIENTED_EDGE('',*,*,#4566,.F.);
#6160=ORIENTED_EDGE('',*,*,#4567,.F.);
#6161=ORIENTED_EDGE('',*,*,#4568,.T.);
#6162=ORIENTED_EDGE('',*,*,#4565,.T.);
#6163=ORIENTED_EDGE('',*,*,#4568,.F.);
#6164=ORIENTED_EDGE('',*,*,#4569,.F.);
#6165=ORIENTED_EDGE('',*,*,#4570,.T.);
#6166=ORIENTED_EDGE('',*,*,#4567,.T.);
#6167=ORIENTED_EDGE('',*,*,#4570,.F.);
#6168=ORIENTED_EDGE('',*,*,#4569,.T.);
#6169=ORIENTED_EDGE('',*,*,#4571,.F.);
#6170=ORIENTED_EDGE('',*,*,#4572,.F.);
#6171=ORIENTED_EDGE('',*,*,#4573,.T.);
#6172=ORIENTED_EDGE('',*,*,#4571,.T.);
#6173=ORIENTED_EDGE('',*,*,#4573,.F.);
#6174=ORIENTED_EDGE('',*,*,#4574,.F.);
#6175=ORIENTED_EDGE('',*,*,#4575,.T.);
#6176=ORIENTED_EDGE('',*,*,#4572,.T.);
#6177=ORIENTED_EDGE('',*,*,#4575,.F.);
#6178=ORIENTED_EDGE('',*,*,#4576,.F.);
#6179=ORIENTED_EDGE('',*,*,#4577,.T.);
#6180=ORIENTED_EDGE('',*,*,#4574,.T.);
#6181=ORIENTED_EDGE('',*,*,#4577,.F.);
#6182=ORIENTED_EDGE('',*,*,#4576,.T.);
#6183=ORIENTED_EDGE('',*,*,#4578,.T.);
#6184=ORIENTED_EDGE('',*,*,#4579,.T.);
#6185=ORIENTED_EDGE('',*,*,#4580,.T.);
#6186=ORIENTED_EDGE('',*,*,#4581,.F.);
#6187=ORIENTED_EDGE('',*,*,#4582,.T.);
#6188=ORIENTED_EDGE('',*,*,#4583,.T.);
#6189=ORIENTED_EDGE('',*,*,#4584,.T.);
#6190=ORIENTED_EDGE('',*,*,#4579,.F.);
#6191=ORIENTED_EDGE('',*,*,#4585,.T.);
#6192=ORIENTED_EDGE('',*,*,#4586,.T.);
#6193=ORIENTED_EDGE('',*,*,#4587,.T.);
#6194=ORIENTED_EDGE('',*,*,#4583,.F.);
#6195=ORIENTED_EDGE('',*,*,#4588,.T.);
#6196=ORIENTED_EDGE('',*,*,#4589,.T.);
#6197=ORIENTED_EDGE('',*,*,#4590,.T.);
#6198=ORIENTED_EDGE('',*,*,#4586,.F.);
#6199=ORIENTED_EDGE('',*,*,#4591,.T.);
#6200=ORIENTED_EDGE('',*,*,#4592,.T.);
#6201=ORIENTED_EDGE('',*,*,#4593,.T.);
#6202=ORIENTED_EDGE('',*,*,#4589,.F.);
#6203=ORIENTED_EDGE('',*,*,#4594,.T.);
#6204=ORIENTED_EDGE('',*,*,#4581,.T.);
#6205=ORIENTED_EDGE('',*,*,#4595,.T.);
#6206=ORIENTED_EDGE('',*,*,#4592,.F.);
#6207=ORIENTED_EDGE('',*,*,#4594,.F.);
#6208=ORIENTED_EDGE('',*,*,#4591,.F.);
#6209=ORIENTED_EDGE('',*,*,#4588,.F.);
#6210=ORIENTED_EDGE('',*,*,#4585,.F.);
#6211=ORIENTED_EDGE('',*,*,#4582,.F.);
#6212=ORIENTED_EDGE('',*,*,#4578,.F.);
#6213=ORIENTED_EDGE('',*,*,#4595,.F.);
#6214=ORIENTED_EDGE('',*,*,#4580,.F.);
#6215=ORIENTED_EDGE('',*,*,#4584,.F.);
#6216=ORIENTED_EDGE('',*,*,#4587,.F.);
#6217=ORIENTED_EDGE('',*,*,#4590,.F.);
#6218=ORIENTED_EDGE('',*,*,#4593,.F.);
#7431=CYLINDRICAL_SURFACE('',#8859,0.35);
#7432=CYLINDRICAL_SURFACE('',#8867,0.1954);
#7819=ADVANCED_FACE('',(#1249),#942,.T.);
#7820=ADVANCED_FACE('',(#1250),#570,.T.);
#7821=ADVANCED_FACE('',(#1251),#7431,.T.);
#7822=ADVANCED_FACE('',(#1252),#571,.T.);
#7823=ADVANCED_FACE('',(#1253,#798),#943,.T.);
#7824=ADVANCED_FACE('',(#1254),#572,.T.);
#7825=ADVANCED_FACE('',(#1255),#7432,.T.);
#7826=ADVANCED_FACE('',(#1256),#573,.T.);
#7827=ADVANCED_FACE('',(#1257),#944,.T.);
#7828=ADVANCED_FACE('',(#1258),#945,.F.);
#7829=ADVANCED_FACE('',(#1259),#946,.F.);
#7830=ADVANCED_FACE('',(#1260),#947,.F.);
#7831=ADVANCED_FACE('',(#1261),#948,.F.);
#7832=ADVANCED_FACE('',(#1262),#949,.F.);
#7833=ADVANCED_FACE('',(#1263),#950,.F.);
#7834=ADVANCED_FACE('',(#1264),#951,.F.);
#7835=ADVANCED_FACE('',(#1265),#952,.F.);
#8079=CLOSED_SHELL('',(#7819,#7820,#7821,#7822,#7823,#7824,#7825,#7826,
#7827));
#8080=CLOSED_SHELL('',(#7828,#7829,#7830,#7831,#7832,#7833,#7834,#7835));
#8854=AXIS2_PLACEMENT_3D('',#14785,#10355,#10356);
#8855=AXIS2_PLACEMENT_3D('',#14786,#10357,#10358);
#8856=AXIS2_PLACEMENT_3D('',#14788,#10359,#10360);
#8857=AXIS2_PLACEMENT_3D('',#14789,#10361,#10362);
#8858=AXIS2_PLACEMENT_3D('',#14791,#10363,#10364);
#8859=AXIS2_PLACEMENT_3D('',#14793,#10366,#10367);
#8860=AXIS2_PLACEMENT_3D('',#14795,#10368,#10369);
#8861=AXIS2_PLACEMENT_3D('',#14797,#10371,#10372);
#8862=AXIS2_PLACEMENT_3D('',#14799,#10373,#10374);
#8863=AXIS2_PLACEMENT_3D('',#14801,#10376,#10377);
#8864=AXIS2_PLACEMENT_3D('',#14803,#10378,#10379);
#8865=AXIS2_PLACEMENT_3D('',#14804,#10380,#10381);
#8866=AXIS2_PLACEMENT_3D('',#14806,#10382,#10383);
#8867=AXIS2_PLACEMENT_3D('',#14808,#10385,#10386);
#8868=AXIS2_PLACEMENT_3D('',#14810,#10387,#10388);
#8869=AXIS2_PLACEMENT_3D('',#14812,#10390,#10391);
#8870=AXIS2_PLACEMENT_3D('',#14814,#10392,#10393);
#8871=AXIS2_PLACEMENT_3D('',#14816,#10395,#10396);
#8872=AXIS2_PLACEMENT_3D('',#14817,#10397,#10398);
#8873=AXIS2_PLACEMENT_3D('',#14826,#10403,#10404);
#8874=AXIS2_PLACEMENT_3D('',#14832,#10408,#10409);
#8875=AXIS2_PLACEMENT_3D('',#14838,#10413,#10414);
#8876=AXIS2_PLACEMENT_3D('',#14844,#10418,#10419);
#8877=AXIS2_PLACEMENT_3D('',#14850,#10423,#10424);
#8878=AXIS2_PLACEMENT_3D('',#14853,#10427,#10428);
#8879=AXIS2_PLACEMENT_3D('',#14854,#10429,#10430);
#10355=DIRECTION('axis',(0.,0.,1.));
#10356=DIRECTION('refdir',(1.,0.,0.));
#10357=DIRECTION('center_axis',(0.,1.,0.));
#10358=DIRECTION('ref_axis',(0.,0.,1.));
#10359=DIRECTION('center_axis',(0.,-1.,0.));
#10360=DIRECTION('ref_axis',(1.,0.,0.));
#10361=DIRECTION('center_axis',(0.,-1.,0.));
#10362=DIRECTION('ref_axis',(1.,0.,0.));
#10363=DIRECTION('center_axis',(0.,-1.,0.));
#10364=DIRECTION('ref_axis',(1.,0.,0.));
#10365=DIRECTION('',(0.707106781186547,0.707106781186548,8.65956056235493E-17));
#10366=DIRECTION('center_axis',(0.,-1.,0.));
#10367=DIRECTION('ref_axis',(1.,0.,0.));
#10368=DIRECTION('center_axis',(0.,-1.,0.));
#10369=DIRECTION('ref_axis',(1.,0.,0.));
#10370=DIRECTION('',(0.,1.,0.));
#10371=DIRECTION('center_axis',(0.,1.,0.));
#10372=DIRECTION('ref_axis',(1.,0.,0.));
#10373=DIRECTION('center_axis',(0.,-1.,0.));
#10374=DIRECTION('ref_axis',(1.,0.,0.));
#10375=DIRECTION('',(-0.707106781186547,0.707106781186548,-8.65956056235493E-17));
#10376=DIRECTION('center_axis',(0.,-1.,0.));
#10377=DIRECTION('ref_axis',(0.,0.,-1.));
#10378=DIRECTION('center_axis',(0.,-1.,0.));
#10379=DIRECTION('ref_axis',(1.,0.,0.));
#10380=DIRECTION('center_axis',(0.,1.,0.));
#10381=DIRECTION('ref_axis',(1.,0.,0.));
#10382=DIRECTION('center_axis',(0.,1.,0.));
#10383=DIRECTION('ref_axis',(1.,0.,0.));
#10384=DIRECTION('',(-0.447213595499958,0.894427190999916,-5.47678698264203E-17));
#10385=DIRECTION('center_axis',(0.,-1.,0.));
#10386=DIRECTION('ref_axis',(1.,0.,0.));
#10387=DIRECTION('center_axis',(0.,1.,0.));
#10388=DIRECTION('ref_axis',(1.,0.,0.));
#10389=DIRECTION('',(0.,1.,0.));
#10390=DIRECTION('center_axis',(0.,1.,0.));
#10391=DIRECTION('ref_axis',(1.,0.,0.));
#10392=DIRECTION('center_axis',(0.,-1.,0.));
#10393=DIRECTION('ref_axis',(1.,0.,0.));
#10394=DIRECTION('',(-0.707106781186547,0.707106781186548,-8.65956056235493E-17));
#10395=DIRECTION('center_axis',(0.,-1.,0.));
#10396=DIRECTION('ref_axis',(0.,0.,-1.));
#10397=DIRECTION('center_axis',(0.866025403784439,0.,-0.5));
#10398=DIRECTION('ref_axis',(0.5,0.,0.866025403784439));
#10399=DIRECTION('',(-0.5,0.,-0.866025403784439));
#10400=DIRECTION('',(0.,-1.,0.));
#10401=DIRECTION('',(0.5,0.,0.866025403784439));
#10402=DIRECTION('',(0.,-1.,0.));
#10403=DIRECTION('center_axis',(1.60246890531964E-16,0.,-1.));
#10404=DIRECTION('ref_axis',(1.,0.,1.60246890531964E-16));
#10405=DIRECTION('',(-1.,0.,-1.60246890531964E-16));
#10406=DIRECTION('',(0.,-1.,0.));
#10407=DIRECTION('',(1.,0.,1.60246890531964E-16));
#10408=DIRECTION('center_axis',(-0.866025403784439,0.,-0.5));
#10409=DIRECTION('ref_axis',(0.5,0.,-0.866025403784439));
#10410=DIRECTION('',(-0.5,0.,0.866025403784439));
#10411=DIRECTION('',(0.,-1.,0.));
#10412=DIRECTION('',(0.5,0.,-0.866025403784439));
#10413=DIRECTION('center_axis',(-0.866025403784439,0.,0.5));
#10414=DIRECTION('ref_axis',(-0.5,0.,-0.866025403784439));
#10415=DIRECTION('',(0.5,0.,0.866025403784439));
#10416=DIRECTION('',(0.,-1.,0.));
#10417=DIRECTION('',(-0.5,0.,-0.866025403784439));
#10418=DIRECTION('center_axis',(-1.60246890531964E-16,0.,1.));
#10419=DIRECTION('ref_axis',(-1.,0.,-1.60246890531964E-16));
#10420=DIRECTION('',(1.,0.,1.60246890531964E-16));
#10421=DIRECTION('',(0.,-1.,0.));
#10422=DIRECTION('',(-1.,0.,-1.60246890531964E-16));
#10423=DIRECTION('center_axis',(0.866025403784439,0.,0.5));
#10424=DIRECTION('ref_axis',(-0.5,0.,0.866025403784439));
#10425=DIRECTION('',(0.5,0.,-0.866025403784439));
#10426=DIRECTION('',(-0.5,0.,0.866025403784439));
#10427=DIRECTION('center_axis',(0.,1.,0.));
#10428=DIRECTION('ref_axis',(1.,0.,0.));
#10429=DIRECTION('center_axis',(0.,-1.,0.));
#10430=DIRECTION('ref_axis',(0.,0.,-1.));
#14785=CARTESIAN_POINT('',(0.,0.,0.));
#14786=CARTESIAN_POINT('Origin',(0.3,0.4,0.));
#14787=CARTESIAN_POINT('',(-0.3,0.4,-3.67394039744206E-17));
#14788=CARTESIAN_POINT('Origin',(0.,0.4,0.));
#14789=CARTESIAN_POINT('Origin',(0.,0.375,0.));
#14790=CARTESIAN_POINT('',(-0.35,0.35,-4.28626379701573E-17));
#14791=CARTESIAN_POINT('Origin',(0.,0.35,0.));
#14792=CARTESIAN_POINT('',(-0.325,0.375,-3.9801020972289E-17));
#14793=CARTESIAN_POINT('Origin',(0.,0.19,0.));
#14794=CARTESIAN_POINT('',(-0.35,0.03,-4.28626379701574E-17));
#14795=CARTESIAN_POINT('Origin',(0.,0.03,0.));
#14796=CARTESIAN_POINT('',(-0.35,0.19,-4.28626379701574E-17));
#14797=CARTESIAN_POINT('Origin',(0.,0.0149999999999999,0.));
#14798=CARTESIAN_POINT('',(-0.32,-3.29597460435593E-17,-3.91886975727153E-17));
#14799=CARTESIAN_POINT('Origin',(0.,0.,0.));
#14800=CARTESIAN_POINT('',(-0.335,0.0149999999999999,-4.10256677714363E-17));
#14801=CARTESIAN_POINT('Origin',(0.22,0.,0.));
#14802=CARTESIAN_POINT('',(-0.22,-6.93889390390723E-18,-2.69422295812418E-17));
#14803=CARTESIAN_POINT('Origin',(0.,0.,0.));
#14804=CARTESIAN_POINT('Origin',(0.,-0.02,0.));
#14805=CARTESIAN_POINT('',(-0.1954,-0.0492,2.39295984553393E-17));
#14806=CARTESIAN_POINT('Origin',(0.,-0.0492,0.));
#14807=CARTESIAN_POINT('',(-0.21,-0.02,-2.57175827820944E-17));
#14808=CARTESIAN_POINT('Origin',(0.,-0.8,0.));
#14809=CARTESIAN_POINT('',(-0.1954,-1.5646,2.39295984553393E-17));
#14810=CARTESIAN_POINT('Origin',(0.,-1.5646,0.));
#14811=CARTESIAN_POINT('',(-0.1954,-0.8,-2.39295984553393E-17));
#14812=CARTESIAN_POINT('Origin',(0.,-1.58,0.));
#14813=CARTESIAN_POINT('',(-0.16,-1.6,-1.95943487863577E-17));
#14814=CARTESIAN_POINT('Origin',(0.,-1.6,0.));
#14815=CARTESIAN_POINT('',(-0.18,-1.58,-2.20436423846524E-17));
#14816=CARTESIAN_POINT('Origin',(0.,-1.6,0.));
#14817=CARTESIAN_POINT('Origin',(0.0866025403784439,-0.4,-0.15));
#14818=CARTESIAN_POINT('',(0.173205080756888,-0.4,0.));
#14819=CARTESIAN_POINT('',(0.0866025403784439,-0.4,-0.15));
#14820=CARTESIAN_POINT('',(0.173205080756888,-0.4,0.));
#14821=CARTESIAN_POINT('',(0.0866025403784439,-0.64,-0.15));
#14822=CARTESIAN_POINT('',(0.0866025403784439,-0.4,-0.15));
#14823=CARTESIAN_POINT('',(0.173205080756888,-0.64,0.));
#14824=CARTESIAN_POINT('',(0.173205080756888,-0.64,0.));
#14825=CARTESIAN_POINT('',(0.173205080756888,-0.4,0.));
#14826=CARTESIAN_POINT('Origin',(-0.0866025403784438,-0.4,-0.15));
#14827=CARTESIAN_POINT('',(-0.0866025403784438,-0.4,-0.15));
#14828=CARTESIAN_POINT('',(0.0866025403784439,-0.4,-0.15));
#14829=CARTESIAN_POINT('',(-0.0866025403784438,-0.64,-0.15));
#14830=CARTESIAN_POINT('',(-0.0866025403784438,-0.4,-0.15));
#14831=CARTESIAN_POINT('',(0.0866025403784439,-0.64,-0.15));
#14832=CARTESIAN_POINT('Origin',(-0.173205080756888,-0.4,-2.77555756156289E-17));
#14833=CARTESIAN_POINT('',(-0.173205080756888,-0.4,-2.12115047744981E-17));
#14834=CARTESIAN_POINT('',(-0.0866025403784438,-0.4,-0.15));
#14835=CARTESIAN_POINT('',(-0.173205080756888,-0.64,-2.77555756156289E-17));
#14836=CARTESIAN_POINT('',(-0.173205080756888,-0.4,-2.12115047744981E-17));
#14837=CARTESIAN_POINT('',(-0.0866025403784438,-0.64,-0.15));
#14838=CARTESIAN_POINT('Origin',(-0.0866025403784439,-0.4,0.15));
#14839=CARTESIAN_POINT('',(-0.0866025403784439,-0.4,0.15));
#14840=CARTESIAN_POINT('',(-0.173205080756888,-0.4,-2.12115047744981E-17));
#14841=CARTESIAN_POINT('',(-0.0866025403784439,-0.64,0.15));
#14842=CARTESIAN_POINT('',(-0.0866025403784439,-0.4,0.15));
#14843=CARTESIAN_POINT('',(-0.173205080756888,-0.64,-2.12115047744981E-17));
#14844=CARTESIAN_POINT('Origin',(0.0866025403784439,-0.4,0.15));
#14845=CARTESIAN_POINT('',(0.0866025403784439,-0.4,0.15));
#14846=CARTESIAN_POINT('',(-0.0866025403784439,-0.4,0.15));
#14847=CARTESIAN_POINT('',(0.0866025403784439,-0.64,0.15));
#14848=CARTESIAN_POINT('',(0.0866025403784439,-0.4,0.15));
#14849=CARTESIAN_POINT('',(-0.0866025403784439,-0.64,0.15));
#14850=CARTESIAN_POINT('Origin',(0.173205080756888,-0.4,0.));
#14851=CARTESIAN_POINT('',(0.0866025403784439,-0.4,0.15));
#14852=CARTESIAN_POINT('',(0.0866025403784439,-0.64,0.15));
#14853=CARTESIAN_POINT('Origin',(0.,-0.4,-2.77555756156289E-17));
#14854=CARTESIAN_POINT('Origin',(0.,-0.64,-2.77555756156289E-17));
#25028=UNCERTAINTY_MEASURE_WITH_UNIT(LENGTH_MEASURE(0.001),#25075,
'DISTANCE_ACCURACY_VALUE',
'Maximum model space distance between geometric entities at asserted c
onnectivities');
#25040=UNCERTAINTY_MEASURE_WITH_UNIT(LENGTH_MEASURE(0.001),#25075,
'DISTANCE_ACCURACY_VALUE',
'Maximum model space distance between geometric entities at asserted c
onnectivities');
#25062=(
GEOMETRIC_REPRESENTATION_CONTEXT(3)
GLOBAL_UNCERTAINTY_ASSIGNED_CONTEXT((#25028))
GLOBAL_UNIT_ASSIGNED_CONTEXT((#25075,#25077,#25078))
REPRESENTATION_CONTEXT('','3D')
);
#25074=(
GEOMETRIC_REPRESENTATION_CONTEXT(3)
GLOBAL_UNCERTAINTY_ASSIGNED_CONTEXT((#25040))
GLOBAL_UNIT_ASSIGNED_CONTEXT((#25075,#25077,#25078))
REPRESENTATION_CONTEXT('','3D')
);
#25075=(
LENGTH_UNIT()
NAMED_UNIT(*)
SI_UNIT(.CENTI.,.METRE.)
);
#25077=(
NAMED_UNIT(*)
PLANE_ANGLE_UNIT()
SI_UNIT($,.RADIAN.)
);
#25078=(
NAMED_UNIT(*)
SI_UNIT($,.STERADIAN.)
SOLID_ANGLE_UNIT()
);
#25100=SHAPE_DEFINITION_REPRESENTATION(#25138,#25215);
#25138=PRODUCT_DEFINITION_SHAPE('',$,#25249);
#25215=SHAPE_REPRESENTATION('',(#8854),#25062);
#25227=PRODUCT_DEFINITION_CONTEXT('part definition',#25328,'design');
#25249=PRODUCT_DEFINITION('Cap Screw - M4x16','Cap Screw - M4x16',#25282,
#25227);
#25282=PRODUCT_DEFINITION_FORMATION('',$,#25351);
#25328=APPLICATION_CONTEXT(
'Core Data for Automotive Mechanical Design Process');
#25329=PRODUCT_CONTEXT('part definition',#25328,'mechanical');
#25351=PRODUCT('Cap Screw - M4x16','Cap Screw - M4x16',
'Cap Screw - M4x16',(#25329));
#25440=COLOUR_RGB('Black',0.12,0.14,0.17);
#25441=FILL_AREA_STYLE_COLOUR('',#25440);
#25442=FILL_AREA_STYLE('',(#25441));
#25443=SURFACE_STYLE_FILL_AREA(#25442);
#25444=SURFACE_SIDE_STYLE('',(#25443));
#25445=SURFACE_STYLE_USAGE(.BOTH.,#25444);
#25446=PRESENTATION_STYLE_ASSIGNMENT((#25445));
ENDSEC;
END-ISO-10303-21;
